ISO-10303-21;
HEADER;
/* Generated by software containing ST-Developer
 * from STEP Tools, Inc. (www.steptools.com) 
 */

FILE_DESCRIPTION(
/* description */ ('Bearing-mounted hook block'),
/* implementation_level */ '2;1');

FILE_NAME(
/* name */ 'Cap Screw - M8x30.step',
/* time_stamp */ '2026-10-28T22:30:11-07:00',
/* author */ (''),
/* organization */ (''),
/* preprocessor_version */ 'ST-DEVELOPER v20.2',
/* originating_system */ 'Autodesk Translation Framework v15.17.0.0',
/* authorisation */ '');

FILE_SCHEMA (('AUTOMOTIVE_DESIGN { 1 0 10303 214 3 1 1 }'));
ENDSEC;

DATA;
#10=MECHANICAL_DESIGN_GEOMETRIC_PRESENTATION_REPRESENTATION('',(#334),#7609);
#256=CONICAL_SURFACE('',#4412,0.625,0.785398163397448);
#257=CONICAL_SURFACE('',#4416,0.635,0.785398163397449);
#258=CONICAL_SURFACE('',#4420,0.41,0.463647609000806);
#259=CONICAL_SURFACE('',#4424,0.36,0.785398163397448);
#270=ORIENTED_CLOSED_SHELL('',*,#3932,.F.);
#273=BREP_WITH_VOIDS('Body1',#3931,(#270));
#286=SHAPE_REPRESENTATION_RELATIONSHIP('SRR','None',#7733,#310);
#310=ADVANCED_BREP_SHAPE_REPRESENTATION('',(#273),#7593);
#334=STYLED_ITEM('',(#7938),#273);
#488=LINE('',#6531,#718);
#489=LINE('',#6535,#719);
#490=LINE('',#6539,#720);
#491=LINE('',#6546,#721);
#492=LINE('',#6550,#722);
#493=LINE('',#6554,#723);
#494=LINE('',#6559,#724);
#495=LINE('',#6561,#725);
#496=LINE('',#6563,#726);
#497=LINE('',#6564,#727);
#498=LINE('',#6567,#728);
#499=LINE('',#6569,#729);
#500=LINE('',#6570,#730);
#501=LINE('',#6573,#731);
#502=LINE('',#6575,#732);
#503=LINE('',#6576,#733);
#504=LINE('',#6579,#734);
#505=LINE('',#6581,#735);
#506=LINE('',#6582,#736);
#507=LINE('',#6585,#737);
#508=LINE('',#6587,#738);
#509=LINE('',#6588,#739);
#510=LINE('',#6590,#740);
#511=LINE('',#6591,#741);
#718=VECTOR('',#5251,0.625);
#719=VECTOR('',#5256,0.65);
#720=VECTOR('',#5261,0.635);
#721=VECTOR('',#5270,0.41);
#722=VECTOR('',#5275,0.4);
#723=VECTOR('',#5280,0.36);
#724=VECTOR('',#5285,1.);
#725=VECTOR('',#5286,1.);
#726=VECTOR('',#5287,1.);
#727=VECTOR('',#5288,1.);
#728=VECTOR('',#5291,1.);
#729=VECTOR('',#5292,1.);
#730=VECTOR('',#5293,1.);
#731=VECTOR('',#5296,1.);
#732=VECTOR('',#5297,1.);
#733=VECTOR('',#5298,1.);
#734=VECTOR('',#5301,1.);
#735=VECTOR('',#5302,1.);
#736=VECTOR('',#5303,1.);
#737=VECTOR('',#5306,1.);
#738=VECTOR('',#5307,1.);
#739=VECTOR('',#5308,1.);
#740=VECTOR('',#5311,1.);
#741=VECTOR('',#5312,1.);
#879=CYLINDRICAL_SURFACE('',#4414,0.65);
#880=CYLINDRICAL_SURFACE('',#4422,0.3933);
#959=FACE_BOUND('',#1374,.T.);
#1095=FACE_OUTER_BOUND('',#1369,.T.);
#1096=FACE_OUTER_BOUND('',#1370,.T.);
#1097=FACE_OUTER_BOUND('',#1371,.T.);
#1098=FACE_OUTER_BOUND('',#1372,.T.);
#1099=FACE_OUTER_BOUND('',#1373,.T.);
#1100=FACE_OUTER_BOUND('',#1375,.T.);
#1101=FACE_OUTER_BOUND('',#1376,.T.);
#1102=FACE_OUTER_BOUND('',#1377,.T.);
#1103=FACE_OUTER_BOUND('',#1378,.T.);
#1104=FACE_OUTER_BOUND('',#1379,.T.);
#1105=FACE_OUTER_BOUND('',#1380,.T.);
#1106=FACE_OUTER_BOUND('',#1381,.T.);
#1107=FACE_OUTER_BOUND('',#1382,.T.);
#1108=FACE_OUTER_BOUND('',#1383,.T.);
#1109=FACE_OUTER_BOUND('',#1384,.T.);
#1110=FACE_OUTER_BOUND('',#1385,.T.);
#1111=FACE_OUTER_BOUND('',#1386,.T.);
#1369=EDGE_LOOP('',(#2988));
#1370=EDGE_LOOP('',(#2989,#2990,#2991,#2992));
#1371=EDGE_LOOP('',(#2993,#2994,#2995,#2996));
#1372=EDGE_LOOP('',(#2997,#2998,#2999,#3000));
#1373=EDGE_LOOP('',(#3001));
#1374=EDGE_LOOP('',(#3002));
#1375=EDGE_LOOP('',(#3003,#3004,#3005,#3006));
#1376=EDGE_LOOP('',(#3007,#3008,#3009,#3010));
#1377=EDGE_LOOP('',(#3011,#3012,#3013,#3014));
#1378=EDGE_LOOP('',(#3015));
#1379=EDGE_LOOP('',(#3016,#3017,#3018,#3019));
#1380=EDGE_LOOP('',(#3020,#3021,#3022,#3023));
#1381=EDGE_LOOP('',(#3024,#3025,#3026,#3027));
#1382=EDGE_LOOP('',(#3028,#3029,#3030,#3031));
#1383=EDGE_LOOP('',(#3032,#3033,#3034,#3035));
#1384=EDGE_LOOP('',(#3036,#3037,#3038,#3039));
#1385=EDGE_LOOP('',(#3040,#3041,#3042,#3043,#3044,#3045));
#1386=EDGE_LOOP('',(#3046,#3047,#3048,#3049,#3050,#3051));
#1636=CIRCLE('',#4411,0.6);
#1637=CIRCLE('',#4413,0.65);
#1638=CIRCLE('',#4415,0.65);
#1639=CIRCLE('',#4417,0.62);
#1640=CIRCLE('',#4419,0.42);
#1641=CIRCLE('',#4421,0.3933);
#1642=CIRCLE('',#4423,0.3933);
#1643=CIRCLE('',#4425,0.32);
#1909=VERTEX_POINT('',#6526);
#1910=VERTEX_POINT('',#6529);
#1911=VERTEX_POINT('',#6533);
#1912=VERTEX_POINT('',#6537);
#1913=VERTEX_POINT('',#6541);
#1914=VERTEX_POINT('',#6544);
#1915=VERTEX_POINT('',#6548);
#1916=VERTEX_POINT('',#6552);
#1917=VERTEX_POINT('',#6557);
#1918=VERTEX_POINT('',#6558);
#1919=VERTEX_POINT('',#6560);
#1920=VERTEX_POINT('',#6562);
#1921=VERTEX_POINT('',#6566);
#1922=VERTEX_POINT('',#6568);
#1923=VERTEX_POINT('',#6572);
#1924=VERTEX_POINT('',#6574);
#1925=VERTEX_POINT('',#6578);
#1926=VERTEX_POINT('',#6580);
#1927=VERTEX_POINT('',#6584);
#1928=VERTEX_POINT('',#6586);
#2304=EDGE_CURVE('',#1909,#1909,#1636,.T.);
#2305=EDGE_CURVE('',#1910,#1910,#1637,.T.);
#2306=EDGE_CURVE('',#1910,#1909,#488,.T.);
#2307=EDGE_CURVE('',#1911,#1911,#1638,.T.);
#2308=EDGE_CURVE('',#1911,#1910,#489,.T.);
#2309=EDGE_CURVE('',#1912,#1912,#1639,.T.);
#2310=EDGE_CURVE('',#1912,#1911,#490,.T.);
#2311=EDGE_CURVE('',#1913,#1913,#1640,.T.);
#2312=EDGE_CURVE('',#1914,#1914,#1641,.F.);
#2313=EDGE_CURVE('',#1914,#1913,#491,.T.);
#2314=EDGE_CURVE('',#1915,#1915,#1642,.F.);
#2315=EDGE_CURVE('',#1915,#1914,#492,.T.);
#2316=EDGE_CURVE('',#1916,#1916,#1643,.T.);
#2317=EDGE_CURVE('',#1916,#1915,#493,.T.);
#2318=EDGE_CURVE('',#1917,#1918,#494,.T.);
#2319=EDGE_CURVE('',#1918,#1919,#495,.T.);
#2320=EDGE_CURVE('',#1919,#1920,#496,.T.);
#2321=EDGE_CURVE('',#1917,#1920,#497,.T.);
#2322=EDGE_CURVE('',#1918,#1921,#498,.T.);
#2323=EDGE_CURVE('',#1921,#1922,#499,.T.);
#2324=EDGE_CURVE('',#1922,#1919,#500,.T.);
#2325=EDGE_CURVE('',#1921,#1923,#501,.T.);
#2326=EDGE_CURVE('',#1923,#1924,#502,.T.);
#2327=EDGE_CURVE('',#1924,#1922,#503,.T.);
#2328=EDGE_CURVE('',#1923,#1925,#504,.T.);
#2329=EDGE_CURVE('',#1925,#1926,#505,.T.);
#2330=EDGE_CURVE('',#1926,#1924,#506,.T.);
#2331=EDGE_CURVE('',#1925,#1927,#507,.T.);
#2332=EDGE_CURVE('',#1927,#1928,#508,.T.);
#2333=EDGE_CURVE('',#1928,#1926,#509,.T.);
#2334=EDGE_CURVE('',#1927,#1917,#510,.T.);
#2335=EDGE_CURVE('',#1920,#1928,#511,.T.);
#2988=ORIENTED_EDGE('',*,*,#2304,.F.);
#2989=ORIENTED_EDGE('',*,*,#2305,.F.);
#2990=ORIENTED_EDGE('',*,*,#2306,.T.);
#2991=ORIENTED_EDGE('',*,*,#2304,.T.);
#2992=ORIENTED_EDGE('',*,*,#2306,.F.);
#2993=ORIENTED_EDGE('',*,*,#2307,.F.);
#2994=ORIENTED_EDGE('',*,*,#2308,.T.);
#2995=ORIENTED_EDGE('',*,*,#2305,.T.);
#2996=ORIENTED_EDGE('',*,*,#2308,.F.);
#2997=ORIENTED_EDGE('',*,*,#2309,.F.);
#2998=ORIENTED_EDGE('',*,*,#2310,.T.);
#2999=ORIENTED_EDGE('',*,*,#2307,.T.);
#3000=ORIENTED_EDGE('',*,*,#2310,.F.);
#3001=ORIENTED_EDGE('',*,*,#2309,.T.);
#3002=ORIENTED_EDGE('',*,*,#2311,.F.);
#3003=ORIENTED_EDGE('',*,*,#2312,.F.);
#3004=ORIENTED_EDGE('',*,*,#2313,.T.);
#3005=ORIENTED_EDGE('',*,*,#2311,.T.);
#3006=ORIENTED_EDGE('',*,*,#2313,.F.);
#3007=ORIENTED_EDGE('',*,*,#2314,.F.);
#3008=ORIENTED_EDGE('',*,*,#2315,.T.);
#3009=ORIENTED_EDGE('',*,*,#2312,.T.);
#3010=ORIENTED_EDGE('',*,*,#2315,.F.);
#3011=ORIENTED_EDGE('',*,*,#2316,.F.);
#3012=ORIENTED_EDGE('',*,*,#2317,.T.);
#3013=ORIENTED_EDGE('',*,*,#2314,.T.);
#3014=ORIENTED_EDGE('',*,*,#2317,.F.);
#3015=ORIENTED_EDGE('',*,*,#2316,.T.);
#3016=ORIENTED_EDGE('',*,*,#2318,.T.);
#3017=ORIENTED_EDGE('',*,*,#2319,.T.);
#3018=ORIENTED_EDGE('',*,*,#2320,.T.);
#3019=ORIENTED_EDGE('',*,*,#2321,.F.);
#3020=ORIENTED_EDGE('',*,*,#2322,.T.);
#3021=ORIENTED_EDGE('',*,*,#2323,.T.);
#3022=ORIENTED_EDGE('',*,*,#2324,.T.);
#3023=ORIENTED_EDGE('',*,*,#2319,.F.);
#3024=ORIENTED_EDGE('',*,*,#2325,.T.);
#3025=ORIENTED_EDGE('',*,*,#2326,.T.);
#3026=ORIENTED_EDGE('',*,*,#2327,.T.);
#3027=ORIENTED_EDGE('',*,*,#2323,.F.);
#3028=ORIENTED_EDGE('',*,*,#2328,.T.);
#3029=ORIENTED_EDGE('',*,*,#2329,.T.);
#3030=ORIENTED_EDGE('',*,*,#2330,.T.);
#3031=ORIENTED_EDGE('',*,*,#2326,.F.);
#3032=ORIENTED_EDGE('',*,*,#2331,.T.);
#3033=ORIENTED_EDGE('',*,*,#2332,.T.);
#3034=ORIENTED_EDGE('',*,*,#2333,.T.);
#3035=ORIENTED_EDGE('',*,*,#2329,.F.);
#3036=ORIENTED_EDGE('',*,*,#2334,.T.);
#3037=ORIENTED_EDGE('',*,*,#2321,.T.);
#3038=ORIENTED_EDGE('',*,*,#2335,.T.);
#3039=ORIENTED_EDGE('',*,*,#2332,.F.);
#3040=ORIENTED_EDGE('',*,*,#2334,.F.);
#3041=ORIENTED_EDGE('',*,*,#2331,.F.);
#3042=ORIENTED_EDGE('',*,*,#2328,.F.);
#3043=ORIENTED_EDGE('',*,*,#2325,.F.);
#3044=ORIENTED_EDGE('',*,*,#2322,.F.);
#3045=ORIENTED_EDGE('',*,*,#2318,.F.);
#3046=ORIENTED_EDGE('',*,*,#2335,.F.);
#3047=ORIENTED_EDGE('',*,*,#2320,.F.);
#3048=ORIENTED_EDGE('',*,*,#2324,.F.);
#3049=ORIENTED_EDGE('',*,*,#2327,.F.);
#3050=ORIENTED_EDGE('',*,*,#2330,.F.);
#3051=ORIENTED_EDGE('',*,*,#2333,.F.);
#3614=PLANE('',#4410);
#3615=PLANE('',#4418);
#3616=PLANE('',#4426);
#3617=PLANE('',#4427);
#3618=PLANE('',#4428);
#3619=PLANE('',#4429);
#3620=PLANE('',#4430);
#3621=PLANE('',#4431);
#3622=PLANE('',#4432);
#3623=PLANE('',#4433);
#3624=PLANE('',#4434);
#3777=ADVANCED_FACE('',(#1095),#3614,.T.);
#3778=ADVANCED_FACE('',(#1096),#256,.T.);
#3779=ADVANCED_FACE('',(#1097),#879,.T.);
#3780=ADVANCED_FACE('',(#1098),#257,.T.);
#3781=ADVANCED_FACE('',(#1099,#959),#3615,.T.);
#3782=ADVANCED_FACE('',(#1100),#258,.T.);
#3783=ADVANCED_FACE('',(#1101),#880,.T.);
#3784=ADVANCED_FACE('',(#1102),#259,.T.);
#3785=ADVANCED_FACE('',(#1103),#3616,.T.);
#3786=ADVANCED_FACE('',(#1104),#3617,.F.);
#3787=ADVANCED_FACE('',(#1105),#3618,.F.);
#3788=ADVANCED_FACE('',(#1106),#3619,.F.);
#3789=ADVANCED_FACE('',(#1107),#3620,.F.);
#3790=ADVANCED_FACE('',(#1108),#3621,.F.);
#3791=ADVANCED_FACE('',(#1109),#3622,.F.);
#3792=ADVANCED_FACE('',(#1110),#3623,.F.);
#3793=ADVANCED_FACE('',(#1111),#3624,.F.);
#3931=CLOSED_SHELL('',(#3777,#3778,#3779,#3780,#3781,#3782,#3783,#3784,
#3785));
#3932=CLOSED_SHELL('',(#3786,#3787,#3788,#3789,#3790,#3791,#3792,#3793));
#4409=AXIS2_PLACEMENT_3D('',#6524,#5241,#5242);
#4410=AXIS2_PLACEMENT_3D('',#6525,#5243,#5244);
#4411=AXIS2_PLACEMENT_3D('',#6527,#5245,#5246);
#4412=AXIS2_PLACEMENT_3D('',#6528,#5247,#5248);
#4413=AXIS2_PLACEMENT_3D('',#6530,#5249,#5250);
#4414=AXIS2_PLACEMENT_3D('',#6532,#5252,#5253);
#4415=AXIS2_PLACEMENT_3D('',#6534,#5254,#5255);
#4416=AXIS2_PLACEMENT_3D('',#6536,#5257,#5258);
#4417=AXIS2_PLACEMENT_3D('',#6538,#5259,#5260);
#4418=AXIS2_PLACEMENT_3D('',#6540,#5262,#5263);
#4419=AXIS2_PLACEMENT_3D('',#6542,#5264,#5265);
#4420=AXIS2_PLACEMENT_3D('',#6543,#5266,#5267);
#4421=AXIS2_PLACEMENT_3D('',#6545,#5268,#5269);
#4422=AXIS2_PLACEMENT_3D('',#6547,#5271,#5272);
#4423=AXIS2_PLACEMENT_3D('',#6549,#5273,#5274);
#4424=AXIS2_PLACEMENT_3D('',#6551,#5276,#5277);
#4425=AXIS2_PLACEMENT_3D('',#6553,#5278,#5279);
#4426=AXIS2_PLACEMENT_3D('',#6555,#5281,#5282);
#4427=AXIS2_PLACEMENT_3D('',#6556,#5283,#5284);
#4428=AXIS2_PLACEMENT_3D('',#6565,#5289,#5290);
#4429=AXIS2_PLACEMENT_3D('',#6571,#5294,#5295);
#4430=AXIS2_PLACEMENT_3D('',#6577,#5299,#5300);
#4431=AXIS2_PLACEMENT_3D('',#6583,#5304,#5305);
#4432=AXIS2_PLACEMENT_3D('',#6589,#5309,#5310);
#4433=AXIS2_PLACEMENT_3D('',#6592,#5313,#5314);
#4434=AXIS2_PLACEMENT_3D('',#6593,#5315,#5316);
#5241=DIRECTION('axis',(0.,0.,1.));
#5242=DIRECTION('refdir',(1.,0.,0.));
#5243=DIRECTION('center_axis',(0.,1.,0.));
#5244=DIRECTION('ref_axis',(0.,0.,1.));
#5245=DIRECTION('center_axis',(0.,-1.,0.));
#5246=DIRECTION('ref_axis',(1.,0.,0.));
#5247=DIRECTION('center_axis',(0.,-1.,0.));
#5248=DIRECTION('ref_axis',(1.,0.,0.));
#5249=DIRECTION('center_axis',(0.,-1.,0.));
#5250=DIRECTION('ref_axis',(1.,0.,0.));
#5251=DIRECTION('',(0.707106781186548,0.707106781186547,8.65956056235493E-17));
#5252=DIRECTION('center_axis',(0.,-1.,0.));
#5253=DIRECTION('ref_axis',(1.,0.,0.));
#5254=DIRECTION('center_axis',(0.,-1.,0.));
#5255=DIRECTION('ref_axis',(1.,0.,0.));
#5256=DIRECTION('',(0.,1.,0.));
#5257=DIRECTION('center_axis',(0.,1.,0.));
#5258=DIRECTION('ref_axis',(1.,0.,0.));
#5259=DIRECTION('center_axis',(0.,-1.,0.));
#5260=DIRECTION('ref_axis',(1.,0.,0.));
#5261=DIRECTION('',(-0.707106781186548,0.707106781186547,-8.65956056235494E-17));
#5262=DIRECTION('center_axis',(0.,-1.,0.));
#5263=DIRECTION('ref_axis',(0.,0.,-1.));
#5264=DIRECTION('center_axis',(0.,-1.,0.));
#5265=DIRECTION('ref_axis',(1.,0.,0.));
#5266=DIRECTION('center_axis',(0.,1.,0.));
#5267=DIRECTION('ref_axis',(1.,0.,0.));
#5268=DIRECTION('center_axis',(0.,1.,0.));
#5269=DIRECTION('ref_axis',(1.,0.,0.));
#5270=DIRECTION('',(-0.447213595499958,0.894427190999916,-5.47678698264203E-17));
#5271=DIRECTION('center_axis',(0.,-1.,0.));
#5272=DIRECTION('ref_axis',(1.,0.,0.));
#5273=DIRECTION('center_axis',(0.,1.,0.));
#5274=DIRECTION('ref_axis',(1.,0.,0.));
#5275=DIRECTION('',(0.,1.,0.));
#5276=DIRECTION('center_axis',(0.,1.,0.));
#5277=DIRECTION('ref_axis',(1.,0.,0.));
#5278=DIRECTION('center_axis',(0.,-1.,0.));
#5279=DIRECTION('ref_axis',(1.,0.,0.));
#5280=DIRECTION('',(-0.707106781186547,0.707106781186548,-8.65956056235493E-17));
#5281=DIRECTION('center_axis',(0.,-1.,0.));
#5282=DIRECTION('ref_axis',(0.,0.,-1.));
#5283=DIRECTION('center_axis',(0.866025403784439,0.,-0.5));
#5284=DIRECTION('ref_axis',(0.5,0.,0.866025403784439));
#5285=DIRECTION('',(-0.5,0.,-0.866025403784439));
#5286=DIRECTION('',(0.,-1.,0.));
#5287=DIRECTION('',(0.5,0.,0.866025403784439));
#5288=DIRECTION('',(0.,-1.,0.));
#5289=DIRECTION('center_axis',(1.60246890531964E-16,0.,-1.));
#5290=DIRECTION('ref_axis',(1.,0.,1.60246890531964E-16));
#5291=DIRECTION('',(-1.,0.,-1.60246890531964E-16));
#5292=DIRECTION('',(0.,-1.,0.));
#5293=DIRECTION('',(1.,0.,1.60246890531964E-16));
#5294=DIRECTION('center_axis',(-0.866025403784439,0.,-0.5));
#5295=DIRECTION('ref_axis',(0.5,0.,-0.866025403784439));
#5296=DIRECTION('',(-0.5,0.,0.866025403784439));
#5297=DIRECTION('',(0.,-1.,0.));
#5298=DIRECTION('',(0.5,0.,-0.866025403784439));
#5299=DIRECTION('center_axis',(-0.866025403784439,0.,0.5));
#5300=DIRECTION('ref_axis',(-0.5,0.,-0.866025403784439));
#5301=DIRECTION('',(0.5,0.,0.866025403784439));
#5302=DIRECTION('',(0.,-1.,0.));
#5303=DIRECTION('',(-0.5,0.,-0.866025403784439));
#5304=DIRECTION('center_axis',(-1.60246890531964E-16,0.,1.));
#5305=DIRECTION('ref_axis',(-1.,0.,-1.60246890531964E-16));
#5306=DIRECTION('',(1.,0.,1.60246890531964E-16));
#5307=DIRECTION('',(0.,-1.,0.));
#5308=DIRECTION('',(-1.,0.,-1.60246890531964E-16));
#5309=DIRECTION('center_axis',(0.866025403784439,0.,0.5));
#5310=DIRECTION('ref_axis',(-0.5,0.,0.866025403784439));
#5311=DIRECTION('',(0.5,0.,-0.866025403784439));
#5312=DIRECTION('',(-0.5,0.,0.866025403784439));
#5313=DIRECTION('center_axis',(0.,1.,0.));
#5314=DIRECTION('ref_axis',(1.,0.,0.));
#5315=DIRECTION('center_axis',(0.,-1.,0.));
#5316=DIRECTION('ref_axis',(0.,0.,-1.));
#6524=CARTESIAN_POINT('',(0.,0.,0.));
#6525=CARTESIAN_POINT('Origin',(0.6,0.8,0.));
#6526=CARTESIAN_POINT('',(-0.6,0.8,-7.34788079488412E-17));
#6527=CARTESIAN_POINT('Origin',(0.,0.8,0.));
#6528=CARTESIAN_POINT('Origin',(0.,0.775,0.));
#6529=CARTESIAN_POINT('',(-0.65,0.75,-7.9602041944578E-17));
#6530=CARTESIAN_POINT('Origin',(0.,0.75,0.));
#6531=CARTESIAN_POINT('',(-0.625,0.775,-7.65404249467096E-17));
#6532=CARTESIAN_POINT('Origin',(0.,0.39,0.));
#6533=CARTESIAN_POINT('',(-0.65,0.0299999999999998,-7.9602041944578E-17));
#6534=CARTESIAN_POINT('Origin',(0.,0.0299999999999998,0.));
#6535=CARTESIAN_POINT('',(-0.65,0.39,-7.9602041944578E-17));
#6536=CARTESIAN_POINT('Origin',(0.,0.0150000000000001,0.));
#6537=CARTESIAN_POINT('',(-0.62,5.89805981832114E-17,-7.59281015471359E-17));
#6538=CARTESIAN_POINT('Origin',(0.,0.,0.));
#6539=CARTESIAN_POINT('',(-0.635,0.0150000000000001,-7.77650717458569E-17));
#6540=CARTESIAN_POINT('Origin',(0.42,0.,0.));
#6541=CARTESIAN_POINT('',(-0.42,-3.46944695195361E-18,-5.14351655641888E-17));
#6542=CARTESIAN_POINT('Origin',(0.,0.,0.));
#6543=CARTESIAN_POINT('Origin',(0.,-0.02,0.));
#6544=CARTESIAN_POINT('',(-0.3933,-0.0534000000000001,4.81653586104654E-17));
#6545=CARTESIAN_POINT('Origin',(0.,-0.0534000000000001,0.));
#6546=CARTESIAN_POINT('',(-0.41,-0.02,-5.02105187650415E-17));
#6547=CARTESIAN_POINT('Origin',(0.,-1.48,0.));
#6548=CARTESIAN_POINT('',(-0.3933,-2.9267,4.81653586104654E-17));
#6549=CARTESIAN_POINT('Origin',(0.,-2.9267,0.));
#6550=CARTESIAN_POINT('',(-0.3933,-1.48,-4.81653586104654E-17));
#6551=CARTESIAN_POINT('Origin',(0.,-2.96,0.));
#6552=CARTESIAN_POINT('',(-0.32,-3.,-3.91886975727153E-17));
#6553=CARTESIAN_POINT('Origin',(0.,-3.,0.));
#6554=CARTESIAN_POINT('',(-0.36,-2.96,-4.40872847693047E-17));
#6555=CARTESIAN_POINT('Origin',(0.,-3.,0.));
#6556=CARTESIAN_POINT('Origin',(0.173205080756888,-0.8,-0.3));
#6557=CARTESIAN_POINT('',(0.346410161513775,-0.8,0.));
#6558=CARTESIAN_POINT('',(0.173205080756888,-0.8,-0.3));
#6559=CARTESIAN_POINT('',(0.346410161513775,-0.8,0.));
#6560=CARTESIAN_POINT('',(0.173205080756888,-1.28,-0.3));
#6561=CARTESIAN_POINT('',(0.173205080756888,-0.8,-0.3));
#6562=CARTESIAN_POINT('',(0.346410161513775,-1.28,0.));
#6563=CARTESIAN_POINT('',(0.346410161513775,-1.28,0.));
#6564=CARTESIAN_POINT('',(0.346410161513775,-0.8,0.));
#6565=CARTESIAN_POINT('Origin',(-0.173205080756888,-0.8,-0.3));
#6566=CARTESIAN_POINT('',(-0.173205080756888,-0.8,-0.3));
#6567=CARTESIAN_POINT('',(0.173205080756888,-0.8,-0.3));
#6568=CARTESIAN_POINT('',(-0.173205080756888,-1.28,-0.3));
#6569=CARTESIAN_POINT('',(-0.173205080756888,-0.8,-0.3));
#6570=CARTESIAN_POINT('',(0.173205080756888,-1.28,-0.3));
#6571=CARTESIAN_POINT('Origin',(-0.346410161513775,-0.8,-5.55111512312578E-17));
#6572=CARTESIAN_POINT('',(-0.346410161513775,-0.8,-4.24230095489963E-17));
#6573=CARTESIAN_POINT('',(-0.173205080756888,-0.8,-0.3));
#6574=CARTESIAN_POINT('',(-0.346410161513775,-1.28,-5.55111512312578E-17));
#6575=CARTESIAN_POINT('',(-0.346410161513775,-0.8,-4.24230095489963E-17));
#6576=CARTESIAN_POINT('',(-0.173205080756888,-1.28,-0.3));
#6577=CARTESIAN_POINT('Origin',(-0.173205080756888,-0.8,0.3));
#6578=CARTESIAN_POINT('',(-0.173205080756888,-0.8,0.3));
#6579=CARTESIAN_POINT('',(-0.346410161513775,-0.8,-4.24230095489963E-17));
#6580=CARTESIAN_POINT('',(-0.173205080756888,-1.28,0.3));
#6581=CARTESIAN_POINT('',(-0.173205080756888,-0.8,0.3));
#6582=CARTESIAN_POINT('',(-0.346410161513775,-1.28,-4.24230095489963E-17));
#6583=CARTESIAN_POINT('Origin',(0.173205080756888,-0.8,0.3));
#6584=CARTESIAN_POINT('',(0.173205080756888,-0.8,0.3));
#6585=CARTESIAN_POINT('',(-0.173205080756888,-0.8,0.3));
#6586=CARTESIAN_POINT('',(0.173205080756888,-1.28,0.3));
#6587=CARTESIAN_POINT('',(0.173205080756888,-0.8,0.3));
#6588=CARTESIAN_POINT('',(-0.173205080756888,-1.28,0.3));
#6589=CARTESIAN_POINT('Origin',(0.346410161513775,-0.8,0.));
#6590=CARTESIAN_POINT('',(0.173205080756888,-0.8,0.3));
#6591=CARTESIAN_POINT('',(0.173205080756888,-1.28,0.3));
#6592=CARTESIAN_POINT('Origin',(0.,-0.8,-5.55111512312578E-17));
#6593=CARTESIAN_POINT('Origin',(0.,-1.28,-5.55111512312578E-17));
#7563=UNCERTAINTY_MEASURE_WITH_UNIT(LENGTH_MEASURE(0.001),#7610,
'DISTANCE_ACCURACY_VALUE',
'Maximum model space distance between geometric entities at asserted c
onnectivities');
#7579=UNCERTAINTY_MEASURE_WITH_UNIT(LENGTH_MEASURE(0.001),#7610,
'DISTANCE_ACCURACY_VALUE',
'Maximum model space distance between geometric entities at asserted c
onnectivities');
#7593=(
GEOMETRIC_REPRESENTATION_CONTEXT(3)
GLOBAL_UNCERTAINTY_ASSIGNED_CONTEXT((#7563))
GLOBAL_UNIT_ASSIGNED_CONTEXT((#7610,#7612,#7613))
REPRESENTATION_CONTEXT('','3D')
);
#7609=(
GEOMETRIC_REPRESENTATION_CONTEXT(3)
GLOBAL_UNCERTAINTY_ASSIGNED_CONTEXT((#7579))
GLOBAL_UNIT_ASSIGNED_CONTEXT((#7610,#7612,#7613))
REPRESENTATION_CONTEXT('','3D')
);
#7610=(
LENGTH_UNIT()
NAMED_UNIT(*)
SI_UNIT(.CENTI.,.METRE.)
);
#7612=(
NAMED_UNIT(*)
PLANE_ANGLE_UNIT()
SI_UNIT($,.RADIAN.)
);
#7613=(
NAMED_UNIT(*)
SI_UNIT($,.STERADIAN.)
SOLID_ANGLE_UNIT()
);
#7627=SHAPE_DEFINITION_REPRESENTATION(#7656,#7733);
#7656=PRODUCT_DEFINITION_SHAPE('',$,#7763);
#7733=SHAPE_REPRESENTATION('',(#4409),#7593);
#7749=PRODUCT_DEFINITION_CONTEXT('part definition',#7838,'design');
#7763=PRODUCT_DEFINITION('Cap Screw - M8x30','Cap Screw - M8x30',#7792,
#7749);
#7792=PRODUCT_DEFINITION_FORMATION('',$,#7853);
#7838=APPLICATION_CONTEXT(
'Core Data for Automotive Mechanical Design Process');
#7839=PRODUCT_CONTEXT('part definition',#7838,'mechanical');
#7853=PRODUCT('Cap Screw - M8x30','Cap Screw - M8x30',
'Cap Screw - M8x30',(#7839));
#7932=COLOUR_RGB('Black',0.12,0.14,0.17);
#7933=FILL_AREA_STYLE_COLOUR('',#7932);
#7934=FILL_AREA_STYLE('',(#7933));
#7935=SURFACE_STYLE_FILL_AREA(#7934);
#7936=SURFACE_SIDE_STYLE('',(#7935));
#7937=SURFACE_STYLE_USAGE(.BOTH.,#7936);
#7938=PRESENTATION_STYLE_ASSIGNMENT((#7937));
ENDSEC;
END-ISO-10303-21;
